ISO-10303-21;
HEADER;
/* Generated by software containing ST-Developer
 * from STEP Tools, Inc. (www.steptools.com) 
 */

FILE_DESCRIPTION(
/* description */ ('PAT-122'),
/* implementation_level */ '2;1');

FILE_NAME(
/* name */ 'Foot (3).step',
/* time_stamp */ '2026-10-29T20:20:12-07:00',
/* author */ (''),
/* organization */ (''),
/* preprocessor_version */ 'ST-DEVELOPER v20.2',
/* originating_system */ 'Autodesk Translation Framework v15.17.0.0',
/* authorisation */ '');

FILE_SCHEMA (('AUTOMOTIVE_DESIGN { 1 0 10303 214 3 1 1 }'));
ENDSEC;

DATA;
#10=MECHANICAL_DESIGN_GEOMETRIC_PRESENTATION_REPRESENTATION('',(#497),#10019);
#453=SHAPE_REPRESENTATION_RELATIONSHIP('SRR','None',#10174,#475);
#475=ADVANCED_BREP_SHAPE_REPRESENTATION('',(#519),#10003);
#497=STYLED_ITEM('',(#10362),#519);
#519=MANIFOLD_SOLID_BREP('Body1',#5619);
#543=FACE_BOUND('',#1156,.T.);
#544=FACE_BOUND('',#1158,.T.);
#621=PLANE('',#5944);
#622=PLANE('',#5945);
#849=FACE_OUTER_BOUND('',#1153,.T.);
#850=FACE_OUTER_BOUND('',#1154,.T.);
#851=FACE_OUTER_BOUND('',#1155,.T.);
#852=FACE_OUTER_BOUND('',#1157,.T.);
#1153=EDGE_LOOP('',(#3937,#3938,#3939,#3940));
#1154=EDGE_LOOP('',(#3941,#3942,#3943,#3944));
#1155=EDGE_LOOP('',(#3945));
#1156=EDGE_LOOP('',(#3946));
#1157=EDGE_LOOP('',(#3947));
#1158=EDGE_LOOP('',(#3948));
#1499=LINE('',#8154,#2043);
#1500=LINE('',#8160,#2044);
#2043=VECTOR('',#6554,0.274999999999999);
#2044=VECTOR('',#6561,2.);
#2599=CIRCLE('',#5939,0.274999999999999);
#2600=CIRCLE('',#5940,0.274999999999999);
#2601=CIRCLE('',#5942,2.);
#2602=CIRCLE('',#5943,2.);
#2729=VERTEX_POINT('',#8151);
#2730=VERTEX_POINT('',#8153);
#2731=VERTEX_POINT('',#8157);
#2732=VERTEX_POINT('',#8159);
#3203=EDGE_CURVE('',#2729,#2729,#2599,.T.);
#3204=EDGE_CURVE('',#2729,#2730,#1499,.T.);
#3205=EDGE_CURVE('',#2730,#2730,#2600,.T.);
#3206=EDGE_CURVE('',#2731,#2731,#2601,.T.);
#3207=EDGE_CURVE('',#2731,#2732,#1500,.T.);
#3208=EDGE_CURVE('',#2732,#2732,#2602,.T.);
#3937=ORIENTED_EDGE('',*,*,#3203,.F.);
#3938=ORIENTED_EDGE('',*,*,#3204,.T.);
#3939=ORIENTED_EDGE('',*,*,#3205,.T.);
#3940=ORIENTED_EDGE('',*,*,#3204,.F.);
#3941=ORIENTED_EDGE('',*,*,#3206,.F.);
#3942=ORIENTED_EDGE('',*,*,#3207,.T.);
#3943=ORIENTED_EDGE('',*,*,#3208,.T.);
#3944=ORIENTED_EDGE('',*,*,#3207,.F.);
#3945=ORIENTED_EDGE('',*,*,#3206,.T.);
#3946=ORIENTED_EDGE('',*,*,#3203,.T.);
#3947=ORIENTED_EDGE('',*,*,#3208,.F.);
#3948=ORIENTED_EDGE('',*,*,#3205,.F.);
#5273=CYLINDRICAL_SURFACE('',#5938,0.274999999999999);
#5274=CYLINDRICAL_SURFACE('',#5941,2.);
#5345=ADVANCED_FACE('',(#849),#5273,.F.);
#5346=ADVANCED_FACE('',(#850),#5274,.T.);
#5347=ADVANCED_FACE('',(#851,#543),#621,.T.);
#5348=ADVANCED_FACE('',(#852,#544),#622,.F.);
#5619=CLOSED_SHELL('',(#5345,#5346,#5347,#5348));
#5937=AXIS2_PLACEMENT_3D('',#8149,#6548,#6549);
#5938=AXIS2_PLACEMENT_3D('',#8150,#6550,#6551);
#5939=AXIS2_PLACEMENT_3D('',#8152,#6552,#6553);
#5940=AXIS2_PLACEMENT_3D('',#8155,#6555,#6556);
#5941=AXIS2_PLACEMENT_3D('',#8156,#6557,#6558);
#5942=AXIS2_PLACEMENT_3D('',#8158,#6559,#6560);
#5943=AXIS2_PLACEMENT_3D('',#8161,#6562,#6563);
#5944=AXIS2_PLACEMENT_3D('',#8162,#6564,#6565);
#5945=AXIS2_PLACEMENT_3D('',#8163,#6566,#6567);
#6548=DIRECTION('axis',(0.,0.,1.));
#6549=DIRECTION('refdir',(1.,0.,0.));
#6550=DIRECTION('center_axis',(0.,0.,1.));
#6551=DIRECTION('ref_axis',(1.,0.,0.));
#6552=DIRECTION('center_axis',(0.,0.,-1.));
#6553=DIRECTION('ref_axis',(1.,0.,0.));
#6554=DIRECTION('',(0.,0.,-1.));
#6555=DIRECTION('center_axis',(0.,0.,-1.));
#6556=DIRECTION('ref_axis',(1.,0.,0.));
#6557=DIRECTION('center_axis',(0.,0.,1.));
#6558=DIRECTION('ref_axis',(1.,0.,0.));
#6559=DIRECTION('center_axis',(0.,0.,1.));
#6560=DIRECTION('ref_axis',(1.,0.,0.));
#6561=DIRECTION('',(0.,0.,-1.));
#6562=DIRECTION('center_axis',(0.,0.,1.));
#6563=DIRECTION('ref_axis',(1.,0.,0.));
#6564=DIRECTION('center_axis',(0.,0.,1.));
#6565=DIRECTION('ref_axis',(1.,0.,0.));
#6566=DIRECTION('center_axis',(0.,0.,1.));
#6567=DIRECTION('ref_axis',(1.,0.,0.));
#8149=CARTESIAN_POINT('',(0.,0.,0.));
#8150=CARTESIAN_POINT('Origin',(19.,19.,-0.8));
#8151=CARTESIAN_POINT('',(18.725,19.,0.));
#8152=CARTESIAN_POINT('Origin',(19.,19.,0.));
#8153=CARTESIAN_POINT('',(18.725,19.,-0.8));
#8154=CARTESIAN_POINT('',(18.725,19.,-0.8));
#8155=CARTESIAN_POINT('Origin',(19.,19.,-0.8));
#8156=CARTESIAN_POINT('Origin',(19.,19.,-0.8));
#8157=CARTESIAN_POINT('',(17.,19.,0.));
#8158=CARTESIAN_POINT('Origin',(19.,19.,0.));
#8159=CARTESIAN_POINT('',(17.,19.,-0.8));
#8160=CARTESIAN_POINT('',(17.,19.,-0.8));
#8161=CARTESIAN_POINT('Origin',(19.,19.,-0.8));
#8162=CARTESIAN_POINT('Origin',(19.,19.,0.));
#8163=CARTESIAN_POINT('Origin',(19.,19.,-0.8));
#9979=UNCERTAINTY_MEASURE_WITH_UNIT(LENGTH_MEASURE(0.001),#10020,
'DISTANCE_ACCURACY_VALUE',
'Maximum model space distance between geometric entities at asserted c
onnectivities');
#9995=UNCERTAINTY_MEASURE_WITH_UNIT(LENGTH_MEASURE(0.001),#10020,
'DISTANCE_ACCURACY_VALUE',
'Maximum model space distance between geometric entities at asserted c
onnectivities');
#10003=(
GEOMETRIC_REPRESENTATION_CONTEXT(3)
GLOBAL_UNCERTAINTY_ASSIGNED_CONTEXT((#9979))
GLOBAL_UNIT_ASSIGNED_CONTEXT((#10020,#10022,#10023))
REPRESENTATION_CONTEXT('','3D')
);
#10019=(
GEOMETRIC_REPRESENTATION_CONTEXT(3)
GLOBAL_UNCERTAINTY_ASSIGNED_CONTEXT((#9995))
GLOBAL_UNIT_ASSIGNED_CONTEXT((#10020,#10022,#10023))
REPRESENTATION_CONTEXT('','3D')
);
#10020=(
LENGTH_UNIT()
NAMED_UNIT(*)
SI_UNIT(.CENTI.,.METRE.)
);
#10022=(
NAMED_UNIT(*)
PLANE_ANGLE_UNIT()
SI_UNIT($,.RADIAN.)
);
#10023=(
NAMED_UNIT(*)
SI_UNIT($,.STERADIAN.)
SOLID_ANGLE_UNIT()
);
#10031=SHAPE_DEFINITION_REPRESENTATION(#10054,#10174);
#10054=PRODUCT_DEFINITION_SHAPE('',$,#10198);
#10174=SHAPE_REPRESENTATION('',(#5937),#10003);
#10190=PRODUCT_DEFINITION_CONTEXT('part definition',#10261,'design');
#10198=PRODUCT_DEFINITION('Foot (3)','Foot (3)',#10221,
#10190);
#10221=PRODUCT_DEFINITION_FORMATION('',$,#10270);
#10261=APPLICATION_CONTEXT(
'Core Data for Automotive Mechanical Design Process');
#10262=PRODUCT_CONTEXT('part definition',#10261,'mechanical');
#10270=PRODUCT('Foot (3)','Foot (3)','Foot (3)',(#10262));
#10356=COLOUR_RGB('Off White',0.89,0.88,0.83);
#10357=FILL_AREA_STYLE_COLOUR('',#10356);
#10358=FILL_AREA_STYLE('',(#10357));
#10359=SURFACE_STYLE_FILL_AREA(#10358);
#10360=SURFACE_SIDE_STYLE('',(#10359));
#10361=SURFACE_STYLE_USAGE(.BOTH.,#10360);
#10362=PRESENTATION_STYLE_ASSIGNMENT((#10361));
ENDSEC;
END-ISO-10303-21;
